ISO-10303-21;
HEADER;
/* Generated by software containing ST-Developer
 * from STEP Tools, Inc. (www.steptools.com) 
 */

FILE_DESCRIPTION(
/* description */ ('STEP AP214'),
/* implementation_level */ '2;1');

FILE_NAME(
/* name */ 'hex bolt gradeab_iso_ISO 4014 - M4 x 25 x 14-N.step',
/* time_stamp */ '2026-10-12T14:05:15-07:00',
/* author */ (''),
/* organization */ (''),
/* preprocessor_version */ 'ST-DEVELOPER v20.2',
/* originating_system */ 'Autodesk Translation Framework v15.15.0.0',
/* authorisation */ '');

FILE_SCHEMA (('AUTOMOTIVE_DESIGN { 1 0 10303 214 3 1 1 }'));
ENDSEC;

DATA;
#10=MECHANICAL_DESIGN_GEOMETRIC_PRESENTATION_REPRESENTATION('',(#289),#39959);
#113=(
BOUNDED_CURVE()
B_SPLINE_CURVE(2,(#39863,#39864,#39865),.UNSPECIFIED.,.F.,.F.)
B_SPLINE_CURVE_WITH_KNOTS((3,3),(-0.935215532485105,-0.564489106699794),
 .UNSPECIFIED.)
CURVE()
GEOMETRIC_REPRESENTATION_ITEM()
RATIONAL_B_SPLINE_CURVE((1.84128182081917,1.84128182081917,1.70908373393142))
REPRESENTATION_ITEM('')
);
#114=(
BOUNDED_CURVE()
B_SPLINE_CURVE(2,(#39866,#39867,#39868),.UNSPECIFIED.,.F.,.F.)
B_SPLINE_CURVE_WITH_KNOTS((3,3),(-1.30594195827042,-0.935215532485105),
 .UNSPECIFIED.)
CURVE()
GEOMETRIC_REPRESENTATION_ITEM()
RATIONAL_B_SPLINE_CURVE((1.70908373393142,1.84128182081917,1.84128182081917))
REPRESENTATION_ITEM('')
);
#115=(
BOUNDED_CURVE()
B_SPLINE_CURVE(2,(#39871,#39872,#39873),.UNSPECIFIED.,.F.,.F.)
B_SPLINE_CURVE_WITH_KNOTS((3,3),(-0.935215532485106,-0.564489106699797),
 .UNSPECIFIED.)
CURVE()
GEOMETRIC_REPRESENTATION_ITEM()
RATIONAL_B_SPLINE_CURVE((1.84128182081917,1.84128182081917,1.70908373393142))
REPRESENTATION_ITEM('')
);
#116=(
BOUNDED_CURVE()
B_SPLINE_CURVE(2,(#39874,#39875,#39876),.UNSPECIFIED.,.F.,.F.)
B_SPLINE_CURVE_WITH_KNOTS((3,3),(-1.30594195827041,-0.935215532485105),
 .UNSPECIFIED.)
CURVE()
GEOMETRIC_REPRESENTATION_ITEM()
RATIONAL_B_SPLINE_CURVE((1.70908373393142,1.84128182081917,1.84128182081917))
REPRESENTATION_ITEM('')
);
#117=(
BOUNDED_CURVE()
B_SPLINE_CURVE(2,(#39879,#39880,#39881),.UNSPECIFIED.,.F.,.F.)
B_SPLINE_CURVE_WITH_KNOTS((3,3),(-1.30594195827042,-0.935215532485106),
 .UNSPECIFIED.)
CURVE()
GEOMETRIC_REPRESENTATION_ITEM()
RATIONAL_B_SPLINE_CURVE((1.70908373393142,1.84128182081917,1.84128182081917))
REPRESENTATION_ITEM('')
);
#118=(
BOUNDED_CURVE()
B_SPLINE_CURVE(2,(#39882,#39883,#39884),.UNSPECIFIED.,.F.,.F.)
B_SPLINE_CURVE_WITH_KNOTS((3,3),(-0.935215532485105,-0.564489106699797),
 .UNSPECIFIED.)
CURVE()
GEOMETRIC_REPRESENTATION_ITEM()
RATIONAL_B_SPLINE_CURVE((1.84128182081917,1.84128182081917,1.70908373393142))
REPRESENTATION_ITEM('')
);
#119=(
BOUNDED_CURVE()
B_SPLINE_CURVE(2,(#39887,#39888,#39889),.UNSPECIFIED.,.F.,.F.)
B_SPLINE_CURVE_WITH_KNOTS((3,3),(-1.30594195827042,-0.935215532485105),
 .UNSPECIFIED.)
CURVE()
GEOMETRIC_REPRESENTATION_ITEM()
RATIONAL_B_SPLINE_CURVE((1.70908373393142,1.84128182081917,1.84128182081917))
REPRESENTATION_ITEM('')
);
#120=(
BOUNDED_CURVE()
B_SPLINE_CURVE(2,(#39890,#39891,#39892),.UNSPECIFIED.,.F.,.F.)
B_SPLINE_CURVE_WITH_KNOTS((3,3),(-0.935215532485106,-0.564489106699794),
 .UNSPECIFIED.)
CURVE()
GEOMETRIC_REPRESENTATION_ITEM()
RATIONAL_B_SPLINE_CURVE((1.84128182081917,1.84128182081918,1.70908373393142))
REPRESENTATION_ITEM('')
);
#121=(
BOUNDED_CURVE()
B_SPLINE_CURVE(2,(#39895,#39896,#39897),.UNSPECIFIED.,.F.,.F.)
B_SPLINE_CURVE_WITH_KNOTS((3,3),(-0.935215532485105,-0.564489106699796),
 .UNSPECIFIED.)
CURVE()
GEOMETRIC_REPRESENTATION_ITEM()
RATIONAL_B_SPLINE_CURVE((1.84128182081917,1.84128182081917,1.70908373393142))
REPRESENTATION_ITEM('')
);
#122=(
BOUNDED_CURVE()
B_SPLINE_CURVE(2,(#39898,#39899,#39900),.UNSPECIFIED.,.F.,.F.)
B_SPLINE_CURVE_WITH_KNOTS((3,3),(-1.30594195827041,-0.935215532485106),
 .UNSPECIFIED.)
CURVE()
GEOMETRIC_REPRESENTATION_ITEM()
RATIONAL_B_SPLINE_CURVE((1.70908373393142,1.84128182081917,1.84128182081917))
REPRESENTATION_ITEM('')
);
#123=(
BOUNDED_CURVE()
B_SPLINE_CURVE(2,(#39903,#39904,#39905),.UNSPECIFIED.,.F.,.F.)
B_SPLINE_CURVE_WITH_KNOTS((3,3),(-1.3059419582704,-0.935215532485106),
 .UNSPECIFIED.)
CURVE()
GEOMETRIC_REPRESENTATION_ITEM()
RATIONAL_B_SPLINE_CURVE((1.70908373393143,1.84128182081917,1.84128182081918))
REPRESENTATION_ITEM('')
);
#124=(
BOUNDED_CURVE()
B_SPLINE_CURVE(2,(#39906,#39907,#39908),.UNSPECIFIED.,.F.,.F.)
B_SPLINE_CURVE_WITH_KNOTS((3,3),(-0.935215532485106,-0.564489106699775),
 .UNSPECIFIED.)
CURVE()
GEOMETRIC_REPRESENTATION_ITEM()
RATIONAL_B_SPLINE_CURVE((1.84128182081917,1.84128182081917,1.70908373393141))
REPRESENTATION_ITEM('')
);
#176=CONICAL_SURFACE('',#19958,1.61,0.785398163397443);
#177=CONICAL_SURFACE('',#19977,3.5,1.0471975511966);
#178=CONICAL_SURFACE('',#19978,3.5,1.0471975511966);
#179=CONICAL_SURFACE('',#19979,3.5,1.0471975511966);
#180=CONICAL_SURFACE('',#19980,3.5,1.0471975511966);
#181=CONICAL_SURFACE('',#19981,3.5,1.0471975511966);
#182=CONICAL_SURFACE('',#19982,3.5,1.0471975511966);
#274=SHAPE_REPRESENTATION_RELATIONSHIP('SRR','None',#40008,#281);
#281=ADVANCED_BREP_SHAPE_REPRESENTATION('',(#296),#39958);
#289=STYLED_ITEM('',(#40046),#296);
#296=MANIFOLD_SOLID_BREP('Body1',#18270);
#861=PLANE('',#19962);
#862=PLANE('',#19963);
#863=PLANE('',#19964);
#864=PLANE('',#19965);
#865=PLANE('',#19966);
#866=PLANE('',#19967);
#867=PLANE('',#19968);
#868=PLANE('',#19969);
#869=PLANE('',#19970);
#870=PLANE('',#19983);
#871=PLANE('',#19984);
#872=PLANE('',#19985);
#873=PLANE('',#19986);
#874=PLANE('',#19987);
#875=PLANE('',#19988);
#1064=FACE_BOUND('',#6976,.T.);
#2960=LINE('',#39807,#4533);
#2961=LINE('',#39818,#4534);
#2962=LINE('',#39821,#4535);
#2963=LINE('',#39826,#4536);
#2964=LINE('',#39827,#4537);
#2965=LINE('',#39830,#4538);
#2966=LINE('',#39831,#4539);
#2967=LINE('',#39834,#4540);
#2968=LINE('',#39835,#4541);
#2969=LINE('',#39838,#4542);
#2970=LINE('',#39839,#4543);
#2971=LINE('',#39842,#4544);
#2972=LINE('',#39843,#4545);
#2973=LINE('',#39846,#4546);
#2974=LINE('',#39847,#4547);
#2975=LINE('',#39910,#4548);
#2976=LINE('',#39911,#4549);
#2977=LINE('',#39913,#4550);
#2978=LINE('',#39915,#4551);
#2979=LINE('',#39917,#4552);
#2980=LINE('',#39919,#4553);
#4533=VECTOR('',#24772,3.5);
#4534=VECTOR('',#24785,1.61);
#4535=VECTOR('',#24790,2.);
#4536=VECTOR('',#24797,1000.);
#4537=VECTOR('',#24798,1000.);
#4538=VECTOR('',#24801,1000.);
#4539=VECTOR('',#24802,1000.);
#4540=VECTOR('',#24805,1000.);
#4541=VECTOR('',#24806,1000.);
#4542=VECTOR('',#24809,1000.);
#4543=VECTOR('',#24810,1000.);
#4544=VECTOR('',#24813,1000.);
#4545=VECTOR('',#24814,1000.);
#4546=VECTOR('',#24817,1000.);
#4547=VECTOR('',#24818,1000.);
#4548=VECTOR('',#24847,1000.);
#4549=VECTOR('',#24848,1000.);
#4550=VECTOR('',#24851,1000.);
#4551=VECTOR('',#24854,1000.);
#4552=VECTOR('',#24857,1000.);
#4553=VECTOR('',#24860,1000.);
#4820=CYLINDRICAL_SURFACE('',#19950,3.5);
#4821=CYLINDRICAL_SURFACE('',#19961,2.);
#5790=FACE_OUTER_BOUND('',#6971,.T.);
#5791=FACE_OUTER_BOUND('',#6972,.T.);
#5792=FACE_OUTER_BOUND('',#6973,.T.);
#5793=FACE_OUTER_BOUND('',#6974,.T.);
#5794=FACE_OUTER_BOUND('',#6975,.T.);
#5795=FACE_OUTER_BOUND('',#6977,.T.);
#5796=FACE_OUTER_BOUND('',#6978,.T.);
#5797=FACE_OUTER_BOUND('',#6979,.T.);
#5798=FACE_OUTER_BOUND('',#6980,.T.);
#5799=FACE_OUTER_BOUND('',#6981,.T.);
#5800=FACE_OUTER_BOUND('',#6982,.T.);
#5801=FACE_OUTER_BOUND('',#6983,.T.);
#5802=FACE_OUTER_BOUND('',#6984,.T.);
#5803=FACE_OUTER_BOUND('',#6985,.T.);
#5804=FACE_OUTER_BOUND('',#6986,.T.);
#5805=FACE_OUTER_BOUND('',#6987,.T.);
#5806=FACE_OUTER_BOUND('',#6988,.T.);
#5807=FACE_OUTER_BOUND('',#6989,.T.);
#5808=FACE_OUTER_BOUND('',#6990,.T.);
#5809=FACE_OUTER_BOUND('',#6991,.T.);
#5810=FACE_OUTER_BOUND('',#6992,.T.);
#5811=FACE_OUTER_BOUND('',#6993,.T.);
#5812=FACE_OUTER_BOUND('',#6994,.T.);
#5813=FACE_OUTER_BOUND('',#6995,.T.);
#5814=FACE_OUTER_BOUND('',#6996,.T.);
#6971=EDGE_LOOP('',(#17148,#17149,#17150,#17151,#17152));
#6972=EDGE_LOOP('',(#17153,#17154,#17155,#17156,#17157,#17158,#17159,#17160,
#17161));
#6973=EDGE_LOOP('',(#17162,#17163,#17164,#17165));
#6974=EDGE_LOOP('',(#17166,#17167,#17168,#17169,#17170));
#6975=EDGE_LOOP('',(#17171));
#6976=EDGE_LOOP('',(#17172));
#6977=EDGE_LOOP('',(#17173));
#6978=EDGE_LOOP('',(#17174,#17175,#17176));
#6979=EDGE_LOOP('',(#17177,#17178,#17179));
#6980=EDGE_LOOP('',(#17180,#17181,#17182));
#6981=EDGE_LOOP('',(#17183,#17184,#17185));
#6982=EDGE_LOOP('',(#17186,#17187,#17188));
#6983=EDGE_LOOP('',(#17189,#17190,#17191));
#6984=EDGE_LOOP('',(#17192,#17193,#17194,#17195,#17196,#17197));
#6985=EDGE_LOOP('',(#17198,#17199,#17200));
#6986=EDGE_LOOP('',(#17201,#17202,#17203));
#6987=EDGE_LOOP('',(#17204,#17205,#17206));
#6988=EDGE_LOOP('',(#17207,#17208,#17209));
#6989=EDGE_LOOP('',(#17210,#17211,#17212));
#6990=EDGE_LOOP('',(#17213,#17214,#17215));
#6991=EDGE_LOOP('',(#17216,#17217,#17218,#17219,#17220,#17221));
#6992=EDGE_LOOP('',(#17222,#17223,#17224,#17225,#17226,#17227));
#6993=EDGE_LOOP('',(#17228,#17229,#17230,#17231,#17232,#17233));
#6994=EDGE_LOOP('',(#17234,#17235,#17236,#17237,#17238,#17239));
#6995=EDGE_LOOP('',(#17240,#17241,#17242,#17243,#17244,#17245));
#6996=EDGE_LOOP('',(#17246,#17247,#17248,#17249,#17250,#17251));
#7657=CIRCLE('',#19946,2.);
#7658=CIRCLE('',#19947,2.);
#7659=CIRCLE('',#19948,0.2);
#7660=CIRCLE('',#19949,2.2);
#7661=CIRCLE('',#19951,3.5);
#7662=CIRCLE('',#19952,3.5);
#7663=CIRCLE('',#19953,3.5);
#7664=CIRCLE('',#19954,3.5);
#7665=CIRCLE('',#19955,3.5);
#7666=CIRCLE('',#19956,3.5);
#7667=CIRCLE('',#19957,3.5);
#7668=CIRCLE('',#19959,2.);
#7669=CIRCLE('',#19960,1.61);
#7670=CIRCLE('',#19971,3.5);
#7671=CIRCLE('',#19972,3.5);
#7672=CIRCLE('',#19973,3.5);
#7673=CIRCLE('',#19974,3.5);
#7674=CIRCLE('',#19975,3.5);
#7675=CIRCLE('',#19976,3.5);
#9353=VERTEX_POINT('',#39791);
#9354=VERTEX_POINT('',#39792);
#9355=VERTEX_POINT('',#39795);
#9356=VERTEX_POINT('',#39799);
#9357=VERTEX_POINT('',#39800);
#9358=VERTEX_POINT('',#39802);
#9359=VERTEX_POINT('',#39804);
#9360=VERTEX_POINT('',#39806);
#9361=VERTEX_POINT('',#39809);
#9362=VERTEX_POINT('',#39811);
#9363=VERTEX_POINT('',#39815);
#9364=VERTEX_POINT('',#39817);
#9365=VERTEX_POINT('',#39825);
#9366=VERTEX_POINT('',#39829);
#9367=VERTEX_POINT('',#39833);
#9368=VERTEX_POINT('',#39837);
#9369=VERTEX_POINT('',#39841);
#9370=VERTEX_POINT('',#39845);
#9371=VERTEX_POINT('',#39849);
#9372=VERTEX_POINT('',#39850);
#9373=VERTEX_POINT('',#39852);
#9374=VERTEX_POINT('',#39854);
#9375=VERTEX_POINT('',#39856);
#9376=VERTEX_POINT('',#39858);
#9377=VERTEX_POINT('',#39862);
#9378=VERTEX_POINT('',#39870);
#9379=VERTEX_POINT('',#39878);
#9380=VERTEX_POINT('',#39886);
#9381=VERTEX_POINT('',#39894);
#9382=VERTEX_POINT('',#39902);
#11954=EDGE_CURVE('',#9353,#9354,#7657,.T.);
#11955=EDGE_CURVE('',#9354,#9353,#7658,.T.);
#11956=EDGE_CURVE('',#9354,#9355,#7659,.T.);
#11957=EDGE_CURVE('',#9355,#9355,#7660,.T.);
#11958=EDGE_CURVE('',#9356,#9357,#7661,.T.);
#11959=EDGE_CURVE('',#9358,#9356,#7662,.T.);
#11960=EDGE_CURVE('',#9359,#9358,#7663,.T.);
#11961=EDGE_CURVE('',#9359,#9360,#2960,.T.);
#11962=EDGE_CURVE('',#9360,#9360,#7664,.T.);
#11963=EDGE_CURVE('',#9361,#9359,#7665,.T.);
#11964=EDGE_CURVE('',#9362,#9361,#7666,.T.);
#11965=EDGE_CURVE('',#9357,#9362,#7667,.T.);
#11966=EDGE_CURVE('',#9363,#9363,#7668,.T.);
#11967=EDGE_CURVE('',#9363,#9364,#2961,.T.);
#11968=EDGE_CURVE('',#9364,#9364,#7669,.T.);
#11969=EDGE_CURVE('',#9353,#9363,#2962,.T.);
#11970=EDGE_CURVE('',#9365,#9361,#2963,.T.);
#11971=EDGE_CURVE('',#9359,#9365,#2964,.T.);
#11972=EDGE_CURVE('',#9361,#9366,#2965,.T.);
#11973=EDGE_CURVE('',#9366,#9362,#2966,.T.);
#11974=EDGE_CURVE('',#9362,#9367,#2967,.T.);
#11975=EDGE_CURVE('',#9367,#9357,#2968,.T.);
#11976=EDGE_CURVE('',#9357,#9368,#2969,.T.);
#11977=EDGE_CURVE('',#9368,#9356,#2970,.T.);
#11978=EDGE_CURVE('',#9356,#9369,#2971,.T.);
#11979=EDGE_CURVE('',#9369,#9358,#2972,.T.);
#11980=EDGE_CURVE('',#9358,#9370,#2973,.T.);
#11981=EDGE_CURVE('',#9370,#9359,#2974,.T.);
#11982=EDGE_CURVE('',#9371,#9372,#7670,.T.);
#11983=EDGE_CURVE('',#9373,#9371,#7671,.T.);
#11984=EDGE_CURVE('',#9374,#9373,#7672,.T.);
#11985=EDGE_CURVE('',#9375,#9374,#7673,.T.);
#11986=EDGE_CURVE('',#9375,#9376,#7674,.T.);
#11987=EDGE_CURVE('',#9372,#9376,#7675,.T.);
#11988=EDGE_CURVE('',#9376,#9377,#113,.T.);
#11989=EDGE_CURVE('',#9377,#9372,#114,.T.);
#11990=EDGE_CURVE('',#9375,#9378,#115,.T.);
#11991=EDGE_CURVE('',#9378,#9376,#116,.T.);
#11992=EDGE_CURVE('',#9379,#9375,#117,.T.);
#11993=EDGE_CURVE('',#9374,#9379,#118,.T.);
#11994=EDGE_CURVE('',#9380,#9374,#119,.T.);
#11995=EDGE_CURVE('',#9373,#9380,#120,.T.);
#11996=EDGE_CURVE('',#9372,#9381,#121,.T.);
#11997=EDGE_CURVE('',#9381,#9371,#122,.T.);
#11998=EDGE_CURVE('',#9382,#9373,#123,.T.);
#11999=EDGE_CURVE('',#9371,#9382,#124,.T.);
#12000=EDGE_CURVE('',#9370,#9382,#2975,.T.);
#12001=EDGE_CURVE('',#9365,#9381,#2976,.T.);
#12002=EDGE_CURVE('',#9369,#9380,#2977,.T.);
#12003=EDGE_CURVE('',#9368,#9379,#2978,.T.);
#12004=EDGE_CURVE('',#9367,#9378,#2979,.T.);
#12005=EDGE_CURVE('',#9366,#9377,#2980,.T.);
#17148=ORIENTED_EDGE('',*,*,#11954,.F.);
#17149=ORIENTED_EDGE('',*,*,#11955,.F.);
#17150=ORIENTED_EDGE('',*,*,#11956,.T.);
#17151=ORIENTED_EDGE('',*,*,#11957,.F.);
#17152=ORIENTED_EDGE('',*,*,#11956,.F.);
#17153=ORIENTED_EDGE('',*,*,#11958,.F.);
#17154=ORIENTED_EDGE('',*,*,#11959,.F.);
#17155=ORIENTED_EDGE('',*,*,#11960,.F.);
#17156=ORIENTED_EDGE('',*,*,#11961,.T.);
#17157=ORIENTED_EDGE('',*,*,#11962,.F.);
#17158=ORIENTED_EDGE('',*,*,#11961,.F.);
#17159=ORIENTED_EDGE('',*,*,#11963,.F.);
#17160=ORIENTED_EDGE('',*,*,#11964,.F.);
#17161=ORIENTED_EDGE('',*,*,#11965,.F.);
#17162=ORIENTED_EDGE('',*,*,#11966,.F.);
#17163=ORIENTED_EDGE('',*,*,#11967,.T.);
#17164=ORIENTED_EDGE('',*,*,#11968,.T.);
#17165=ORIENTED_EDGE('',*,*,#11967,.F.);
#17166=ORIENTED_EDGE('',*,*,#11954,.T.);
#17167=ORIENTED_EDGE('',*,*,#11955,.T.);
#17168=ORIENTED_EDGE('',*,*,#11969,.T.);
#17169=ORIENTED_EDGE('',*,*,#11966,.T.);
#17170=ORIENTED_EDGE('',*,*,#11969,.F.);
#17171=ORIENTED_EDGE('',*,*,#11962,.T.);
#17172=ORIENTED_EDGE('',*,*,#11957,.T.);
#17173=ORIENTED_EDGE('',*,*,#11968,.F.);
#17174=ORIENTED_EDGE('',*,*,#11970,.T.);
#17175=ORIENTED_EDGE('',*,*,#11963,.T.);
#17176=ORIENTED_EDGE('',*,*,#11971,.T.);
#17177=ORIENTED_EDGE('',*,*,#11972,.T.);
#17178=ORIENTED_EDGE('',*,*,#11973,.T.);
#17179=ORIENTED_EDGE('',*,*,#11964,.T.);
#17180=ORIENTED_EDGE('',*,*,#11974,.T.);
#17181=ORIENTED_EDGE('',*,*,#11975,.T.);
#17182=ORIENTED_EDGE('',*,*,#11965,.T.);
#17183=ORIENTED_EDGE('',*,*,#11976,.T.);
#17184=ORIENTED_EDGE('',*,*,#11977,.T.);
#17185=ORIENTED_EDGE('',*,*,#11958,.T.);
#17186=ORIENTED_EDGE('',*,*,#11978,.T.);
#17187=ORIENTED_EDGE('',*,*,#11979,.T.);
#17188=ORIENTED_EDGE('',*,*,#11959,.T.);
#17189=ORIENTED_EDGE('',*,*,#11980,.T.);
#17190=ORIENTED_EDGE('',*,*,#11981,.T.);
#17191=ORIENTED_EDGE('',*,*,#11960,.T.);
#17192=ORIENTED_EDGE('',*,*,#11982,.F.);
#17193=ORIENTED_EDGE('',*,*,#11983,.F.);
#17194=ORIENTED_EDGE('',*,*,#11984,.F.);
#17195=ORIENTED_EDGE('',*,*,#11985,.F.);
#17196=ORIENTED_EDGE('',*,*,#11986,.T.);
#17197=ORIENTED_EDGE('',*,*,#11987,.F.);
#17198=ORIENTED_EDGE('',*,*,#11988,.T.);
#17199=ORIENTED_EDGE('',*,*,#11989,.T.);
#17200=ORIENTED_EDGE('',*,*,#11987,.T.);
#17201=ORIENTED_EDGE('',*,*,#11990,.T.);
#17202=ORIENTED_EDGE('',*,*,#11991,.T.);
#17203=ORIENTED_EDGE('',*,*,#11986,.F.);
#17204=ORIENTED_EDGE('',*,*,#11992,.T.);
#17205=ORIENTED_EDGE('',*,*,#11985,.T.);
#17206=ORIENTED_EDGE('',*,*,#11993,.T.);
#17207=ORIENTED_EDGE('',*,*,#11994,.T.);
#17208=ORIENTED_EDGE('',*,*,#11984,.T.);
#17209=ORIENTED_EDGE('',*,*,#11995,.T.);
#17210=ORIENTED_EDGE('',*,*,#11996,.T.);
#17211=ORIENTED_EDGE('',*,*,#11997,.T.);
#17212=ORIENTED_EDGE('',*,*,#11982,.T.);
#17213=ORIENTED_EDGE('',*,*,#11998,.T.);
#17214=ORIENTED_EDGE('',*,*,#11983,.T.);
#17215=ORIENTED_EDGE('',*,*,#11999,.T.);
#17216=ORIENTED_EDGE('',*,*,#11981,.F.);
#17217=ORIENTED_EDGE('',*,*,#12000,.T.);
#17218=ORIENTED_EDGE('',*,*,#11999,.F.);
#17219=ORIENTED_EDGE('',*,*,#11997,.F.);
#17220=ORIENTED_EDGE('',*,*,#12001,.F.);
#17221=ORIENTED_EDGE('',*,*,#11971,.F.);
#17222=ORIENTED_EDGE('',*,*,#11979,.F.);
#17223=ORIENTED_EDGE('',*,*,#12002,.T.);
#17224=ORIENTED_EDGE('',*,*,#11995,.F.);
#17225=ORIENTED_EDGE('',*,*,#11998,.F.);
#17226=ORIENTED_EDGE('',*,*,#12000,.F.);
#17227=ORIENTED_EDGE('',*,*,#11980,.F.);
#17228=ORIENTED_EDGE('',*,*,#11977,.F.);
#17229=ORIENTED_EDGE('',*,*,#12003,.T.);
#17230=ORIENTED_EDGE('',*,*,#11993,.F.);
#17231=ORIENTED_EDGE('',*,*,#11994,.F.);
#17232=ORIENTED_EDGE('',*,*,#12002,.F.);
#17233=ORIENTED_EDGE('',*,*,#11978,.F.);
#17234=ORIENTED_EDGE('',*,*,#11975,.F.);
#17235=ORIENTED_EDGE('',*,*,#12004,.T.);
#17236=ORIENTED_EDGE('',*,*,#11990,.F.);
#17237=ORIENTED_EDGE('',*,*,#11992,.F.);
#17238=ORIENTED_EDGE('',*,*,#12003,.F.);
#17239=ORIENTED_EDGE('',*,*,#11976,.F.);
#17240=ORIENTED_EDGE('',*,*,#11973,.F.);
#17241=ORIENTED_EDGE('',*,*,#12005,.T.);
#17242=ORIENTED_EDGE('',*,*,#11988,.F.);
#17243=ORIENTED_EDGE('',*,*,#11991,.F.);
#17244=ORIENTED_EDGE('',*,*,#12004,.F.);
#17245=ORIENTED_EDGE('',*,*,#11974,.F.);
#17246=ORIENTED_EDGE('',*,*,#11970,.F.);
#17247=ORIENTED_EDGE('',*,*,#12001,.T.);
#17248=ORIENTED_EDGE('',*,*,#11996,.F.);
#17249=ORIENTED_EDGE('',*,*,#11989,.F.);
#17250=ORIENTED_EDGE('',*,*,#12005,.F.);
#17251=ORIENTED_EDGE('',*,*,#11972,.F.);
#17261=TOROIDAL_SURFACE('',#19945,2.2,0.2);
#18234=ADVANCED_FACE('',(#5790),#17261,.F.);
#18235=ADVANCED_FACE('',(#5791),#4820,.T.);
#18236=ADVANCED_FACE('',(#5792),#176,.T.);
#18237=ADVANCED_FACE('',(#5793),#4821,.T.);
#18238=ADVANCED_FACE('',(#5794,#1064),#861,.T.);
#18239=ADVANCED_FACE('',(#5795),#862,.F.);
#18240=ADVANCED_FACE('',(#5796),#863,.T.);
#18241=ADVANCED_FACE('',(#5797),#864,.T.);
#18242=ADVANCED_FACE('',(#5798),#865,.T.);
#18243=ADVANCED_FACE('',(#5799),#866,.T.);
#18244=ADVANCED_FACE('',(#5800),#867,.T.);
#18245=ADVANCED_FACE('',(#5801),#868,.T.);
#18246=ADVANCED_FACE('',(#5802),#869,.F.);
#18247=ADVANCED_FACE('',(#5803),#177,.T.);
#18248=ADVANCED_FACE('',(#5804),#178,.T.);
#18249=ADVANCED_FACE('',(#5805),#179,.T.);
#18250=ADVANCED_FACE('',(#5806),#180,.T.);
#18251=ADVANCED_FACE('',(#5807),#181,.T.);
#18252=ADVANCED_FACE('',(#5808),#182,.T.);
#18253=ADVANCED_FACE('',(#5809),#870,.F.);
#18254=ADVANCED_FACE('',(#5810),#871,.F.);
#18255=ADVANCED_FACE('',(#5811),#872,.F.);
#18256=ADVANCED_FACE('',(#5812),#873,.F.);
#18257=ADVANCED_FACE('',(#5813),#874,.F.);
#18258=ADVANCED_FACE('',(#5814),#875,.F.);
#18270=CLOSED_SHELL('',(#18234,#18235,#18236,#18237,#18238,#18239,#18240,
#18241,#18242,#18243,#18244,#18245,#18246,#18247,#18248,#18249,#18250,#18251,
#18252,#18253,#18254,#18255,#18256,#18257,#18258));
#19944=AXIS2_PLACEMENT_3D('',#39789,#24752,#24753);
#19945=AXIS2_PLACEMENT_3D('',#39790,#24754,#24755);
#19946=AXIS2_PLACEMENT_3D('',#39793,#24756,#24757);
#19947=AXIS2_PLACEMENT_3D('',#39794,#24758,#24759);
#19948=AXIS2_PLACEMENT_3D('',#39796,#24760,#24761);
#19949=AXIS2_PLACEMENT_3D('',#39797,#24762,#24763);
#19950=AXIS2_PLACEMENT_3D('',#39798,#24764,#24765);
#19951=AXIS2_PLACEMENT_3D('',#39801,#24766,#24767);
#19952=AXIS2_PLACEMENT_3D('',#39803,#24768,#24769);
#19953=AXIS2_PLACEMENT_3D('',#39805,#24770,#24771);
#19954=AXIS2_PLACEMENT_3D('',#39808,#24773,#24774);
#19955=AXIS2_PLACEMENT_3D('',#39810,#24775,#24776);
#19956=AXIS2_PLACEMENT_3D('',#39812,#24777,#24778);
#19957=AXIS2_PLACEMENT_3D('',#39813,#24779,#24780);
#19958=AXIS2_PLACEMENT_3D('',#39814,#24781,#24782);
#19959=AXIS2_PLACEMENT_3D('',#39816,#24783,#24784);
#19960=AXIS2_PLACEMENT_3D('',#39819,#24786,#24787);
#19961=AXIS2_PLACEMENT_3D('',#39820,#24788,#24789);
#19962=AXIS2_PLACEMENT_3D('',#39822,#24791,#24792);
#19963=AXIS2_PLACEMENT_3D('',#39823,#24793,#24794);
#19964=AXIS2_PLACEMENT_3D('',#39824,#24795,#24796);
#19965=AXIS2_PLACEMENT_3D('',#39828,#24799,#24800);
#19966=AXIS2_PLACEMENT_3D('',#39832,#24803,#24804);
#19967=AXIS2_PLACEMENT_3D('',#39836,#24807,#24808);
#19968=AXIS2_PLACEMENT_3D('',#39840,#24811,#24812);
#19969=AXIS2_PLACEMENT_3D('',#39844,#24815,#24816);
#19970=AXIS2_PLACEMENT_3D('',#39848,#24819,#24820);
#19971=AXIS2_PLACEMENT_3D('',#39851,#24821,#24822);
#19972=AXIS2_PLACEMENT_3D('',#39853,#24823,#24824);
#19973=AXIS2_PLACEMENT_3D('',#39855,#24825,#24826);
#19974=AXIS2_PLACEMENT_3D('',#39857,#24827,#24828);
#19975=AXIS2_PLACEMENT_3D('',#39859,#24829,#24830);
#19976=AXIS2_PLACEMENT_3D('',#39860,#24831,#24832);
#19977=AXIS2_PLACEMENT_3D('',#39861,#24833,#24834);
#19978=AXIS2_PLACEMENT_3D('',#39869,#24835,#24836);
#19979=AXIS2_PLACEMENT_3D('',#39877,#24837,#24838);
#19980=AXIS2_PLACEMENT_3D('',#39885,#24839,#24840);
#19981=AXIS2_PLACEMENT_3D('',#39893,#24841,#24842);
#19982=AXIS2_PLACEMENT_3D('',#39901,#24843,#24844);
#19983=AXIS2_PLACEMENT_3D('',#39909,#24845,#24846);
#19984=AXIS2_PLACEMENT_3D('',#39912,#24849,#24850);
#19985=AXIS2_PLACEMENT_3D('',#39914,#24852,#24853);
#19986=AXIS2_PLACEMENT_3D('',#39916,#24855,#24856);
#19987=AXIS2_PLACEMENT_3D('',#39918,#24858,#24859);
#19988=AXIS2_PLACEMENT_3D('',#39920,#24861,#24862);
#24752=DIRECTION('axis',(0.,0.,1.));
#24753=DIRECTION('refdir',(1.,0.,0.));
#24754=DIRECTION('center_axis',(1.,0.,0.));
#24755=DIRECTION('ref_axis',(0.,0.,-1.));
#24756=DIRECTION('center_axis',(1.,0.,0.));
#24757=DIRECTION('ref_axis',(0.,0.,-1.));
#24758=DIRECTION('center_axis',(1.,0.,0.));
#24759=DIRECTION('ref_axis',(0.,0.,-1.));
#24760=DIRECTION('center_axis',(0.,1.,1.22464679914735E-16));
#24761=DIRECTION('ref_axis',(0.,-1.22464679914735E-16,1.));
#24762=DIRECTION('center_axis',(-1.,0.,0.));
#24763=DIRECTION('ref_axis',(0.,0.,-1.));
#24764=DIRECTION('center_axis',(-1.,0.,0.));
#24765=DIRECTION('ref_axis',(0.,0.,1.));
#24766=DIRECTION('center_axis',(-1.,0.,0.));
#24767=DIRECTION('ref_axis',(0.,0.,1.));
#24768=DIRECTION('center_axis',(-1.,0.,0.));
#24769=DIRECTION('ref_axis',(0.,0.,1.));
#24770=DIRECTION('center_axis',(-1.,0.,0.));
#24771=DIRECTION('ref_axis',(0.,0.,1.));
#24772=DIRECTION('',(1.,0.,0.));
#24773=DIRECTION('center_axis',(1.,0.,0.));
#24774=DIRECTION('ref_axis',(0.,0.,-1.));
#24775=DIRECTION('center_axis',(-1.,0.,0.));
#24776=DIRECTION('ref_axis',(0.,0.,1.));
#24777=DIRECTION('center_axis',(-1.,0.,0.));
#24778=DIRECTION('ref_axis',(0.,0.,1.));
#24779=DIRECTION('center_axis',(-1.,0.,0.));
#24780=DIRECTION('ref_axis',(0.,0.,1.));
#24781=DIRECTION('center_axis',(-1.,0.,0.));
#24782=DIRECTION('ref_axis',(0.,0.,1.));
#24783=DIRECTION('center_axis',(-1.,0.,0.));
#24784=DIRECTION('ref_axis',(0.,0.,1.));
#24785=DIRECTION('',(0.707106781186551,8.65956056235488E-17,0.707106781186544));
#24786=DIRECTION('center_axis',(-1.,0.,0.));
#24787=DIRECTION('ref_axis',(0.,0.,1.));
#24788=DIRECTION('center_axis',(-1.,0.,0.));
#24789=DIRECTION('ref_axis',(0.,0.,1.));
#24790=DIRECTION('',(1.,0.,0.));
#24791=DIRECTION('center_axis',(1.,0.,0.));
#24792=DIRECTION('ref_axis',(0.,0.,-1.));
#24793=DIRECTION('center_axis',(-1.,0.,0.));
#24794=DIRECTION('ref_axis',(0.,0.,1.));
#24795=DIRECTION('center_axis',(1.,0.,0.));
#24796=DIRECTION('ref_axis',(0.,0.,-1.));
#24797=DIRECTION('',(0.,0.500000000000001,0.866025403784438));
#24798=DIRECTION('',(0.,1.,1.07308185624083E-16));
#24799=DIRECTION('center_axis',(1.,0.,0.));
#24800=DIRECTION('ref_axis',(0.,0.,-1.));
#24801=DIRECTION('',(0.,0.500000000000001,0.866025403784438));
#24802=DIRECTION('',(0.,-0.500000000000001,0.866025403784438));
#24803=DIRECTION('center_axis',(1.,0.,0.));
#24804=DIRECTION('ref_axis',(0.,0.,-1.));
#24805=DIRECTION('',(0.,-0.500000000000001,0.866025403784438));
#24806=DIRECTION('',(0.,-1.,0.));
#24807=DIRECTION('center_axis',(1.,0.,0.));
#24808=DIRECTION('ref_axis',(0.,0.,-1.));
#24809=DIRECTION('',(0.,-1.,0.));
#24810=DIRECTION('',(0.,-0.500000000000002,-0.866025403784437));
#24811=DIRECTION('center_axis',(1.,0.,0.));
#24812=DIRECTION('ref_axis',(0.,0.,-1.));
#24813=DIRECTION('',(0.,-0.500000000000002,-0.866025403784437));
#24814=DIRECTION('',(0.,0.5,-0.866025403784438));
#24815=DIRECTION('center_axis',(1.,0.,0.));
#24816=DIRECTION('ref_axis',(0.,0.,-1.));
#24817=DIRECTION('',(0.,0.5,-0.866025403784438));
#24818=DIRECTION('',(0.,1.,1.07308185624083E-16));
#24819=DIRECTION('center_axis',(1.,0.,0.));
#24820=DIRECTION('ref_axis',(0.,0.,-1.));
#24821=DIRECTION('center_axis',(1.,0.,0.));
#24822=DIRECTION('ref_axis',(0.,0.,-1.));
#24823=DIRECTION('center_axis',(1.,0.,0.));
#24824=DIRECTION('ref_axis',(0.,0.,-1.));
#24825=DIRECTION('center_axis',(1.,0.,0.));
#24826=DIRECTION('ref_axis',(0.,0.,-1.));
#24827=DIRECTION('center_axis',(1.,0.,0.));
#24828=DIRECTION('ref_axis',(0.,0.,-1.));
#24829=DIRECTION('center_axis',(-1.,0.,0.));
#24830=DIRECTION('ref_axis',(0.,0.,1.));
#24831=DIRECTION('center_axis',(1.,0.,0.));
#24832=DIRECTION('ref_axis',(0.,0.,-1.));
#24833=DIRECTION('center_axis',(1.,0.,0.));
#24834=DIRECTION('ref_axis',(0.,0.,-1.));
#24835=DIRECTION('center_axis',(1.,0.,0.));
#24836=DIRECTION('ref_axis',(0.,0.,-1.));
#24837=DIRECTION('center_axis',(1.,0.,0.));
#24838=DIRECTION('ref_axis',(0.,0.,-1.));
#24839=DIRECTION('center_axis',(1.,0.,0.));
#24840=DIRECTION('ref_axis',(0.,0.,-1.));
#24841=DIRECTION('center_axis',(1.,0.,0.));
#24842=DIRECTION('ref_axis',(0.,0.,-1.));
#24843=DIRECTION('center_axis',(1.,0.,0.));
#24844=DIRECTION('ref_axis',(0.,0.,-1.));
#24845=DIRECTION('center_axis',(0.,-1.07308185624083E-16,1.));
#24846=DIRECTION('ref_axis',(0.,-1.,-1.07308185624083E-16));
#24847=DIRECTION('',(-1.,0.,0.));
#24848=DIRECTION('',(-1.,0.,0.));
#24849=DIRECTION('center_axis',(0.,0.866025403784438,0.5));
#24850=DIRECTION('ref_axis',(0.,-0.5,0.866025403784438));
#24851=DIRECTION('',(-1.,0.,0.));
#24852=DIRECTION('center_axis',(0.,0.866025403784438,-0.500000000000002));
#24853=DIRECTION('ref_axis',(0.,0.500000000000002,0.866025403784438));
#24854=DIRECTION('',(-1.,0.,0.));
#24855=DIRECTION('center_axis',(0.,0.,-1.));
#24856=DIRECTION('ref_axis',(-1.,0.,0.));
#24857=DIRECTION('',(-1.,0.,0.));
#24858=DIRECTION('center_axis',(0.,-0.866025403784438,-0.500000000000001));
#24859=DIRECTION('ref_axis',(0.,0.500000000000001,-0.866025403784438));
#24860=DIRECTION('',(-1.,0.,0.));
#24861=DIRECTION('center_axis',(0.,-0.866025403784438,0.500000000000001));
#24862=DIRECTION('ref_axis',(0.,-0.500000000000001,-0.866025403784438));
#39789=CARTESIAN_POINT('',(0.,0.,0.));
#39790=CARTESIAN_POINT('Origin',(3.,0.,0.));
#39791=CARTESIAN_POINT('',(3.,2.44929359829471E-16,-2.));
#39792=CARTESIAN_POINT('',(3.,-2.44929359829471E-16,2.));
#39793=CARTESIAN_POINT('Origin',(3.,0.,0.));
#39794=CARTESIAN_POINT('Origin',(3.,0.,0.));
#39795=CARTESIAN_POINT('',(2.8,-2.69422295812418E-16,2.2));
#39796=CARTESIAN_POINT('Origin',(3.,-2.69422295812418E-16,2.2));
#39797=CARTESIAN_POINT('Origin',(2.8,0.,0.));
#39798=CARTESIAN_POINT('Origin',(0.,0.,0.));
#39799=CARTESIAN_POINT('',(2.4,-3.03108891324553,1.75000000000001));
#39800=CARTESIAN_POINT('',(2.4,0.,3.5));
#39801=CARTESIAN_POINT('Origin',(2.4,0.,0.));
#39802=CARTESIAN_POINT('',(2.4,-3.03108891324553,-1.75));
#39803=CARTESIAN_POINT('Origin',(2.4,0.,0.));
#39804=CARTESIAN_POINT('',(2.4,3.7557864968429E-16,-3.5));
#39805=CARTESIAN_POINT('Origin',(2.4,0.,0.));
#39806=CARTESIAN_POINT('',(2.8,-4.28626379701574E-16,-3.5));
#39807=CARTESIAN_POINT('',(0.,-4.28626379701574E-16,-3.5));
#39808=CARTESIAN_POINT('Origin',(2.8,0.,0.));
#39809=CARTESIAN_POINT('',(2.4,3.03108891324553,-1.75));
#39810=CARTESIAN_POINT('Origin',(2.4,0.,0.));
#39811=CARTESIAN_POINT('',(2.4,3.03108891324553,1.75));
#39812=CARTESIAN_POINT('Origin',(2.4,0.,0.));
#39813=CARTESIAN_POINT('Origin',(2.4,0.,0.));
#39814=CARTESIAN_POINT('Origin',(27.8,0.,0.));
#39815=CARTESIAN_POINT('',(27.41,-2.44929359829471E-16,-2.));
#39816=CARTESIAN_POINT('Origin',(27.41,0.,0.));
#39817=CARTESIAN_POINT('',(27.8,-1.97168134662724E-16,-1.61));
#39818=CARTESIAN_POINT('',(27.8,-1.97168134662724E-16,-1.61));
#39819=CARTESIAN_POINT('Origin',(27.8,0.,0.));
#39820=CARTESIAN_POINT('Origin',(0.,0.,0.));
#39821=CARTESIAN_POINT('',(0.,-2.44929359829471E-16,-2.));
#39822=CARTESIAN_POINT('Origin',(2.8,4.04145188432738,0.));
#39823=CARTESIAN_POINT('Origin',(27.8,0.,0.));
#39824=CARTESIAN_POINT('Origin',(2.4,3.5,0.));
#39825=CARTESIAN_POINT('',(2.4,2.02072594216369,-3.5));
#39826=CARTESIAN_POINT('',(2.4,2.02072594216369,-3.5));
#39827=CARTESIAN_POINT('',(2.4,2.02072594216369,-3.5));
#39828=CARTESIAN_POINT('Origin',(2.4,3.5,0.));
#39829=CARTESIAN_POINT('',(2.4,4.04145188432738,0.));
#39830=CARTESIAN_POINT('',(2.4,2.02072594216369,-3.5));
#39831=CARTESIAN_POINT('',(2.4,4.04145188432738,0.));
#39832=CARTESIAN_POINT('Origin',(2.4,3.5,0.));
#39833=CARTESIAN_POINT('',(2.4,2.02072594216369,3.5));
#39834=CARTESIAN_POINT('',(2.4,4.04145188432738,0.));
#39835=CARTESIAN_POINT('',(2.4,2.02072594216369,3.5));
#39836=CARTESIAN_POINT('Origin',(2.4,3.5,0.));
#39837=CARTESIAN_POINT('',(2.4,-2.02072594216369,3.5));
#39838=CARTESIAN_POINT('',(2.4,2.02072594216369,3.5));
#39839=CARTESIAN_POINT('',(2.4,-4.04145188432739,0.));
#39840=CARTESIAN_POINT('Origin',(2.4,3.5,0.));
#39841=CARTESIAN_POINT('',(2.4,-4.04145188432739,0.));
#39842=CARTESIAN_POINT('',(2.4,-4.04145188432739,0.));
#39843=CARTESIAN_POINT('',(2.4,-2.0207259421637,-3.5));
#39844=CARTESIAN_POINT('Origin',(2.4,3.5,0.));
#39845=CARTESIAN_POINT('',(2.4,-2.0207259421637,-3.5));
#39846=CARTESIAN_POINT('',(2.4,-2.0207259421637,-3.5));
#39847=CARTESIAN_POINT('',(2.4,2.02072594216369,-3.5));
#39848=CARTESIAN_POINT('Origin',(0.,4.04145188432738,0.));
#39849=CARTESIAN_POINT('',(0.,3.7557864968429E-16,-3.5));
#39850=CARTESIAN_POINT('',(0.,3.03108891324553,-1.75));
#39851=CARTESIAN_POINT('Origin',(0.,0.,0.));
#39852=CARTESIAN_POINT('',(0.,-3.03108891324553,-1.75));
#39853=CARTESIAN_POINT('Origin',(0.,0.,0.));
#39854=CARTESIAN_POINT('',(0.,-3.03108891324553,1.75000000000001));
#39855=CARTESIAN_POINT('Origin',(0.,0.,0.));
#39856=CARTESIAN_POINT('',(0.,0.,3.5));
#39857=CARTESIAN_POINT('Origin',(0.,0.,0.));
#39858=CARTESIAN_POINT('',(0.,3.03108891324553,1.75));
#39859=CARTESIAN_POINT('Origin',(0.,0.,0.));
#39860=CARTESIAN_POINT('Origin',(0.,0.,0.));
#39861=CARTESIAN_POINT('Origin',(0.,0.,0.));
#39862=CARTESIAN_POINT('',(0.312607391169643,4.04145188432738,-2.66911020840508E-16));
#39863=CARTESIAN_POINT('Ctrl Pts',(-4.82369624061666E-16,3.03108891324553,
1.75));
#39864=CARTESIAN_POINT('Ctrl Pts',(-2.22044604925031E-16,3.5000000000009,
0.937822173507365));
#39865=CARTESIAN_POINT('Ctrl Pts',(0.312607391170941,4.04145188432963,-3.89552910831185E-12));
#39866=CARTESIAN_POINT('Ctrl Pts',(0.312607391170943,4.04145188432964,3.89877711483892E-12));
#39867=CARTESIAN_POINT('Ctrl Pts',(3.62259049097696E-16,3.5000000000009,
-0.937822173507367));
#39868=CARTESIAN_POINT('Ctrl Pts',(9.64739248123335E-16,3.03108891324553,
-1.75000000000001));
#39869=CARTESIAN_POINT('Origin',(0.,0.,0.));
#39870=CARTESIAN_POINT('',(0.31260739116964,2.02072594216368,3.5));
#39871=CARTESIAN_POINT('Ctrl Pts',(4.82369624061667E-16,-3.85895699249333E-15,
3.5));
#39872=CARTESIAN_POINT('Ctrl Pts',(-2.77555756156289E-17,0.937822173510732,
3.5));
#39873=CARTESIAN_POINT('Ctrl Pts',(0.312607391170938,2.02072594216818,3.5));
#39874=CARTESIAN_POINT('Ctrl Pts',(0.312607391170937,2.02072594216144,3.50000000000389));
#39875=CARTESIAN_POINT('Ctrl Pts',(-8.6328561492913E-16,2.56217782649016,
2.56217782649263));
#39876=CARTESIAN_POINT('Ctrl Pts',(-4.82369624061666E-16,3.03108891324553,
1.75));
#39877=CARTESIAN_POINT('Origin',(0.,0.,0.));
#39878=CARTESIAN_POINT('',(0.312607391169641,-2.02072594216369,3.5));
#39879=CARTESIAN_POINT('Ctrl Pts',(0.312607391170939,-2.02072594216818,
3.5));
#39880=CARTESIAN_POINT('Ctrl Pts',(1.03932589631759E-15,-0.937822173510737,
3.5));
#39881=CARTESIAN_POINT('Ctrl Pts',(4.82369624061667E-16,-3.85895699249333E-15,
3.5));
#39882=CARTESIAN_POINT('Ctrl Pts',(1.74858988722354E-15,-3.03108891324553,
1.75000000000001));
#39883=CARTESIAN_POINT('Ctrl Pts',(2.55351295663786E-15,-2.56217782649016,
2.56217782649264));
#39884=CARTESIAN_POINT('Ctrl Pts',(0.312607391170939,-2.02072594216144,
3.5000000000039));
#39885=CARTESIAN_POINT('Origin',(0.,0.,0.));
#39886=CARTESIAN_POINT('',(0.312607391169646,-4.04145188432739,1.06150963257362E-16));
#39887=CARTESIAN_POINT('Ctrl Pts',(0.312607391170944,-4.04145188432964,
-3.89461966648427E-12));
#39888=CARTESIAN_POINT('Ctrl Pts',(1.05543578901031E-15,-3.5000000000009,
0.937822173507371));
#39889=CARTESIAN_POINT('Ctrl Pts',(1.74858988722354E-15,-3.03108891324553,
1.75000000000001));
#39890=CARTESIAN_POINT('Ctrl Pts',(2.83392154136229E-15,-3.03108891324554,
-1.75000000000001));
#39891=CARTESIAN_POINT('Ctrl Pts',(1.97064586870965E-15,-3.50000000000091,
-0.937822173507369));
#39892=CARTESIAN_POINT('Ctrl Pts',(0.312607391170943,-4.04145188432964,
3.89397006517885E-12));
#39893=CARTESIAN_POINT('Origin',(0.,0.,0.));
#39894=CARTESIAN_POINT('',(0.31260739116964,2.02072594216369,-3.5));
#39895=CARTESIAN_POINT('Ctrl Pts',(9.64739248123335E-16,3.03108891324553,
-1.75000000000001));
#39896=CARTESIAN_POINT('Ctrl Pts',(1.52655665885959E-15,2.56217782649016,
-2.56217782649264));
#39897=CARTESIAN_POINT('Ctrl Pts',(0.312607391170938,2.02072594216144,-3.50000000000389));
#39898=CARTESIAN_POINT('Ctrl Pts',(0.312607391170937,2.02072594216818,-3.5));
#39899=CARTESIAN_POINT('Ctrl Pts',(4.11322098714103E-16,0.937822173510735,
-3.5));
#39900=CARTESIAN_POINT('Ctrl Pts',(-1.20592406015415E-16,3.85895699249333E-15,
-3.5));
#39901=CARTESIAN_POINT('Origin',(0.,0.,0.));
#39902=CARTESIAN_POINT('',(0.312607391169536,-2.02072594216386,-3.5));
#39903=CARTESIAN_POINT('Ctrl Pts',(0.312607391170909,-2.0207259421615,-3.5000000000038));
#39904=CARTESIAN_POINT('Ctrl Pts',(3.55895681952653E-15,-2.56217782649019,
-2.5621778264926));
#39905=CARTESIAN_POINT('Ctrl Pts',(2.83392154136229E-15,-3.03108891324554,
-1.75000000000001));
#39906=CARTESIAN_POINT('Ctrl Pts',(-1.20592406015415E-16,3.85895699249333E-15,
-3.5));
#39907=CARTESIAN_POINT('Ctrl Pts',(-5.82867087928207E-16,-0.937822173510786,
-3.5));
#39908=CARTESIAN_POINT('Ctrl Pts',(0.312607391170976,-2.02072594216831,
-3.5));
#39909=CARTESIAN_POINT('Origin',(2.8,2.02072594216369,-3.5));
#39910=CARTESIAN_POINT('',(2.8,-2.0207259421637,-3.5));
#39911=CARTESIAN_POINT('',(2.8,2.02072594216369,-3.5));
#39912=CARTESIAN_POINT('Origin',(2.8,-2.0207259421637,-3.5));
#39913=CARTESIAN_POINT('',(2.8,-4.04145188432739,0.));
#39914=CARTESIAN_POINT('Origin',(2.8,-4.04145188432739,0.));
#39915=CARTESIAN_POINT('',(2.8,-2.02072594216369,3.5));
#39916=CARTESIAN_POINT('Origin',(2.8,2.02072594216369,3.5));
#39917=CARTESIAN_POINT('',(2.8,2.02072594216369,3.5));
#39918=CARTESIAN_POINT('Origin',(2.8,4.04145188432738,0.));
#39919=CARTESIAN_POINT('',(2.8,4.04145188432738,0.));
#39920=CARTESIAN_POINT('Origin',(2.8,2.02072594216369,-3.5));
#39949=UNCERTAINTY_MEASURE_WITH_UNIT(LENGTH_MEASURE(0.01),#39960,
'DISTANCE_ACCURACY_VALUE',
'Maximum model space distance between geometric entities at asserted c
onnectivities');
#39950=UNCERTAINTY_MEASURE_WITH_UNIT(LENGTH_MEASURE(0.01),#39960,
'DISTANCE_ACCURACY_VALUE',
'Maximum model space distance between geometric entities at asserted c
onnectivities');
#39958=(
GEOMETRIC_REPRESENTATION_CONTEXT(3)
GLOBAL_UNCERTAINTY_ASSIGNED_CONTEXT((#39949))
GLOBAL_UNIT_ASSIGNED_CONTEXT((#39960,#39962,#39963))
REPRESENTATION_CONTEXT('','3D')
);
#39959=(
GEOMETRIC_REPRESENTATION_CONTEXT(3)
GLOBAL_UNCERTAINTY_ASSIGNED_CONTEXT((#39950))
GLOBAL_UNIT_ASSIGNED_CONTEXT((#39960,#39962,#39963))
REPRESENTATION_CONTEXT('','3D')
);
#39960=(
LENGTH_UNIT()
NAMED_UNIT(*)
SI_UNIT(.MILLI.,.METRE.)
);
#39962=(
NAMED_UNIT(*)
PLANE_ANGLE_UNIT()
SI_UNIT($,.RADIAN.)
);
#39963=(
NAMED_UNIT(*)
SI_UNIT($,.STERADIAN.)
SOLID_ANGLE_UNIT()
);
#39971=SHAPE_DEFINITION_REPRESENTATION(#39979,#40008);
#39979=PRODUCT_DEFINITION_SHAPE('',$,#40017);
#40008=SHAPE_REPRESENTATION('',(#19944),#39958);
#40009=PRODUCT_DEFINITION_CONTEXT('part definition',#40035,'design');
#40017=PRODUCT_DEFINITION(
'hex bolt gradeab_iso_ISO 4014 - M4 x 25 x 14-N',
'hex bolt gradeab_iso_ISO 4014 - M4 x 25 x 14-N',#40025,#40009);
#40025=PRODUCT_DEFINITION_FORMATION('',$,#40044);
#40035=APPLICATION_CONTEXT(
'Core Data for Automotive Mechanical Design Process');
#40036=PRODUCT_CONTEXT('part definition',#40035,'mechanical');
#40044=PRODUCT('hex bolt gradeab_iso_ISO 4014 - M4 x 25 x 14-N',
'hex bolt gradeab_iso_ISO 4014 - M4 x 25 x 14-N',$,(#40036));
#40046=PRESENTATION_STYLE_ASSIGNMENT((#40048));
#40048=SURFACE_STYLE_USAGE(.BOTH.,#40050);
#40050=SURFACE_SIDE_STYLE('',(#40052));
#40052=SURFACE_STYLE_FILL_AREA(#40054);
#40054=FILL_AREA_STYLE('Opaque(202,209,238)',(#40056));
#40056=FILL_AREA_STYLE_COLOUR('Opaque(202,209,238)',#40058);
#40058=COLOUR_RGB('Opaque(202,209,238)', 0.66274510, 0.83137255, 0.94901961);
ENDSEC;
END-ISO-10303-21;
